ISO-10303-21;
HEADER;
/* Generated by software containing ST-Developer
 * from STEP Tools, Inc. (www.steptools.com) 
 */

FILE_DESCRIPTION(
/* description */ ('', 'CAx-IF Rec.Pracs.---Representation and Presentation of Product Manufa
cturing Information (PMI)---4.0---2014-10-13'),
/* implementation_level */ '2;1');

FILE_NAME(
/* name */ 'Retaining Ring _ Washer.step',
/* time_stamp */ '2026-10-28T14:45:12+01:00',
/* author */ (''),
/* organization */ (''),
/* preprocessor_version */ 'ST-DEVELOPER v20.2',
/* originating_system */ 'Autodesk Translation Framework v15.17.0.0',
/* authorisation */ '');

FILE_SCHEMA (('AP242_MANAGED_MODEL_BASED_3D_ENGINEERING_MIM_LF { 1 0 10303 442 2 1 4 }'));
ENDSEC;

DATA;
#10=MECHANICAL_DESIGN_GEOMETRIC_PRESENTATION_REPRESENTATION('',(#269),#52164);
#243=SHAPE_REPRESENTATION_RELATIONSHIP('SRR','None',#52222,#256);
#256=ADVANCED_BREP_SHAPE_REPRESENTATION('',(#282),#52162);
#269=STYLED_ITEM('',(#52325),#282);
#282=MANIFOLD_SOLID_BREP('Body1',#9129);
#320=FACE_BOUND('',#1616,.T.);
#321=FACE_BOUND('',#1619,.T.);
#515=PLANE('',#10176);
#516=PLANE('',#10181);
#1046=FACE_OUTER_BOUND('',#1615,.T.);
#1047=FACE_OUTER_BOUND('',#1617,.T.);
#1048=FACE_OUTER_BOUND('',#1618,.T.);
#1049=FACE_OUTER_BOUND('',#1620,.T.);
#1615=EDGE_LOOP('',(#8318));
#1616=EDGE_LOOP('',(#8319));
#1617=EDGE_LOOP('',(#8320,#8321,#8322,#8323));
#1618=EDGE_LOOP('',(#8324));
#1619=EDGE_LOOP('',(#8325));
#1620=EDGE_LOOP('',(#8326,#8327,#8328,#8329));
#2083=CIRCLE('',#10177,3.8);
#2084=CIRCLE('',#10178,2.5);
#2085=CIRCLE('',#10180,2.5);
#2086=CIRCLE('',#10182,3.8);
#2923=LINE('',#52093,#3388);
#2924=LINE('',#52099,#3389);
#3388=VECTOR('',#12481,2.5);
#3389=VECTOR('',#12490,3.8);
#4245=VERTEX_POINT('',#52087);
#4246=VERTEX_POINT('',#52089);
#4247=VERTEX_POINT('',#52092);
#4248=VERTEX_POINT('',#52096);
#5605=EDGE_CURVE('',#4245,#4245,#2083,.T.);
#5606=EDGE_CURVE('',#4246,#4246,#2084,.T.);
#5607=EDGE_CURVE('',#4246,#4247,#2923,.T.);
#5608=EDGE_CURVE('',#4247,#4247,#2085,.T.);
#5609=EDGE_CURVE('',#4248,#4248,#2086,.T.);
#5610=EDGE_CURVE('',#4248,#4245,#2924,.T.);
#8318=ORIENTED_EDGE('',*,*,#5605,.F.);
#8319=ORIENTED_EDGE('',*,*,#5606,.F.);
#8320=ORIENTED_EDGE('',*,*,#5606,.T.);
#8321=ORIENTED_EDGE('',*,*,#5607,.T.);
#8322=ORIENTED_EDGE('',*,*,#5608,.F.);
#8323=ORIENTED_EDGE('',*,*,#5607,.F.);
#8324=ORIENTED_EDGE('',*,*,#5609,.T.);
#8325=ORIENTED_EDGE('',*,*,#5608,.T.);
#8326=ORIENTED_EDGE('',*,*,#5609,.F.);
#8327=ORIENTED_EDGE('',*,*,#5610,.T.);
#8328=ORIENTED_EDGE('',*,*,#5605,.T.);
#8329=ORIENTED_EDGE('',*,*,#5610,.F.);
#8577=CYLINDRICAL_SURFACE('',#10179,2.5);
#8578=CYLINDRICAL_SURFACE('',#10183,3.8);
#9109=ADVANCED_FACE('',(#1046,#320),#515,.F.);
#9110=ADVANCED_FACE('',(#1047),#8577,.F.);
#9111=ADVANCED_FACE('',(#1048,#321),#516,.T.);
#9112=ADVANCED_FACE('',(#1049),#8578,.T.);
#9129=CLOSED_SHELL('',(#9109,#9110,#9111,#9112));
#10175=AXIS2_PLACEMENT_3D('',#52085,#12471,#12472);
#10176=AXIS2_PLACEMENT_3D('',#52086,#12473,#12474);
#10177=AXIS2_PLACEMENT_3D('',#52088,#12475,#12476);
#10178=AXIS2_PLACEMENT_3D('',#52090,#12477,#12478);
#10179=AXIS2_PLACEMENT_3D('',#52091,#12479,#12480);
#10180=AXIS2_PLACEMENT_3D('',#52094,#12482,#12483);
#10181=AXIS2_PLACEMENT_3D('',#52095,#12484,#12485);
#10182=AXIS2_PLACEMENT_3D('',#52097,#12486,#12487);
#10183=AXIS2_PLACEMENT_3D('',#52098,#12488,#12489);
#12471=DIRECTION('axis',(0.,0.,1.));
#12472=DIRECTION('refdir',(1.,0.,0.));
#12473=DIRECTION('center_axis',(0.,1.,0.));
#12474=DIRECTION('ref_axis',(1.,0.,0.));
#12475=DIRECTION('center_axis',(0.,1.,0.));
#12476=DIRECTION('ref_axis',(1.,0.,0.));
#12477=DIRECTION('center_axis',(0.,-1.,0.));
#12478=DIRECTION('ref_axis',(1.,0.,0.));
#12479=DIRECTION('center_axis',(0.,1.,0.));
#12480=DIRECTION('ref_axis',(1.,0.,0.));
#12481=DIRECTION('',(0.,1.,0.));
#12482=DIRECTION('center_axis',(0.,-1.,0.));
#12483=DIRECTION('ref_axis',(1.,0.,0.));
#12484=DIRECTION('center_axis',(0.,1.,0.));
#12485=DIRECTION('ref_axis',(1.,0.,0.));
#12486=DIRECTION('center_axis',(0.,1.,0.));
#12487=DIRECTION('ref_axis',(1.,0.,0.));
#12488=DIRECTION('center_axis',(0.,1.,0.));
#12489=DIRECTION('ref_axis',(1.,0.,0.));
#12490=DIRECTION('',(0.,-1.,0.));
#52085=CARTESIAN_POINT('',(0.,0.,0.));
#52086=CARTESIAN_POINT('Origin',(0.,0.,0.));
#52087=CARTESIAN_POINT('',(-3.8,0.,4.65365783675994E-16));
#52088=CARTESIAN_POINT('Origin',(0.,0.,0.));
#52089=CARTESIAN_POINT('',(-2.5,0.,3.06161699786838E-16));
#52090=CARTESIAN_POINT('Origin',(0.,0.,0.));
#52091=CARTESIAN_POINT('Origin',(0.,0.,0.));
#52092=CARTESIAN_POINT('',(-2.5,2.,3.06161699786838E-16));
#52093=CARTESIAN_POINT('',(-2.5,0.,3.06161699786838E-16));
#52094=CARTESIAN_POINT('Origin',(0.,2.,0.));
#52095=CARTESIAN_POINT('Origin',(0.,2.,0.));
#52096=CARTESIAN_POINT('',(-3.8,2.,4.65365783675994E-16));
#52097=CARTESIAN_POINT('Origin',(0.,2.,0.));
#52098=CARTESIAN_POINT('Origin',(0.,0.,0.));
#52099=CARTESIAN_POINT('',(-3.8,0.,4.65365783675994E-16));
#52147=UNCERTAINTY_MEASURE_WITH_UNIT(LENGTH_MEASURE(0.01),#52165,
'DISTANCE_ACCURACY_VALUE',
'Maximum model space distance between geometric entities at asserted c
onnectivities');
#52149=UNCERTAINTY_MEASURE_WITH_UNIT(LENGTH_MEASURE(0.01),#52165,
'DISTANCE_ACCURACY_VALUE',
'Maximum model space distance between geometric entities at asserted c
onnectivities');
#52162=(
GEOMETRIC_REPRESENTATION_CONTEXT(3)
GLOBAL_UNCERTAINTY_ASSIGNED_CONTEXT((#52147))
GLOBAL_UNIT_ASSIGNED_CONTEXT((#52165,#52167,#52168))
REPRESENTATION_CONTEXT('','3D')
);
#52164=(
GEOMETRIC_REPRESENTATION_CONTEXT(3)
GLOBAL_UNCERTAINTY_ASSIGNED_CONTEXT((#52149))
GLOBAL_UNIT_ASSIGNED_CONTEXT((#52165,#52167,#52168))
REPRESENTATION_CONTEXT('','3D')
);
#52165=(
LENGTH_UNIT()
NAMED_UNIT(*)
SI_UNIT(.MILLI.,.METRE.)
);
#52167=(
NAMED_UNIT(*)
PLANE_ANGLE_UNIT()
SI_UNIT($,.RADIAN.)
);
#52168=(
NAMED_UNIT(*)
SI_UNIT($,.STERADIAN.)
SOLID_ANGLE_UNIT()
);
#52181=SHAPE_DEFINITION_REPRESENTATION(#52195,#52222);
#52195=PRODUCT_DEFINITION_SHAPE('',$,#52237);
#52222=SHAPE_REPRESENTATION('',(#10175),#52162);
#52224=PRODUCT_DEFINITION_CONTEXT('part definition',#52268,'design');
#52237=PRODUCT_DEFINITION('Retaining Ring / Washer',
'Retaining Ring / Washer',#52251,#52224);
#52251=PRODUCT_DEFINITION_FORMATION('',$,#52282);
#52268=APPLICATION_CONTEXT('Managed model based 3d engineering');
#52269=PRODUCT_CONTEXT('part definition',#52268,'mechanical');
#52282=PRODUCT('Retaining Ring / Washer','Retaining Ring / Washer',
'NOT SPECIFIED',(#52269));
#52319=COLOUR_RGB('Black',0.12,0.14,0.17);
#52320=FILL_AREA_STYLE_COLOUR('',#52319);
#52321=FILL_AREA_STYLE('',(#52320));
#52322=SURFACE_STYLE_FILL_AREA(#52321);
#52323=SURFACE_SIDE_STYLE('',(#52322));
#52324=SURFACE_STYLE_USAGE(.BOTH.,#52323);
#52325=PRESENTATION_STYLE_ASSIGNMENT((#52324));
ENDSEC;
END-ISO-10303-21;
